ISO-10303-21;
HEADER;
/* Generated by software containing ST-Developer
 * from STEP Tools, Inc. (www.steptools.com) 
 */

FILE_DESCRIPTION(
/* description */ ('Union bypass pipe loop'),
/* implementation_level */ '2;1');

FILE_NAME(
/* name */ 'Flat Washer - M8.step',
/* time_stamp */ '2026-10-27T21:00:29-07:00',
/* author */ (''),
/* organization */ (''),
/* preprocessor_version */ 'ST-DEVELOPER v20.2',
/* originating_system */ 'Autodesk Translation Framework v15.17.0.0',
/* authorisation */ '');

FILE_SCHEMA (('AUTOMOTIVE_DESIGN { 1 0 10303 214 3 1 1 }'));
ENDSEC;

DATA;
#10=MECHANICAL_DESIGN_GEOMETRIC_PRESENTATION_REPRESENTATION('',(#469),#10095);
#405=SHAPE_REPRESENTATION_RELATIONSHIP('SRR','None',#10274,#437);
#437=ADVANCED_BREP_SHAPE_REPRESENTATION('',(#498),#10086);
#469=STYLED_ITEM('',(#10507),#498);
#498=MANIFOLD_SOLID_BREP('Body1',#5543);
#622=FACE_BOUND('',#1533,.T.);
#623=FACE_BOUND('',#1535,.T.);
#771=PLANE('',#6458);
#772=PLANE('',#6459);
#1087=FACE_OUTER_BOUND('',#1530,.T.);
#1088=FACE_OUTER_BOUND('',#1531,.T.);
#1089=FACE_OUTER_BOUND('',#1532,.T.);
#1090=FACE_OUTER_BOUND('',#1534,.T.);
#1530=EDGE_LOOP('',(#4748,#4749,#4750,#4751));
#1531=EDGE_LOOP('',(#4752,#4753,#4754,#4755));
#1532=EDGE_LOOP('',(#4756));
#1533=EDGE_LOOP('',(#4757));
#1534=EDGE_LOOP('',(#4758));
#1535=EDGE_LOOP('',(#4759));
#1884=LINE('',#9601,#2260);
#1885=LINE('',#9607,#2261);
#2260=VECTOR('',#7978,0.42);
#2261=VECTOR('',#7985,0.8);
#2591=CIRCLE('',#6453,0.42);
#2592=CIRCLE('',#6454,0.42);
#2593=CIRCLE('',#6456,0.8);
#2594=CIRCLE('',#6457,0.8);
#2960=VERTEX_POINT('',#9598);
#2961=VERTEX_POINT('',#9600);
#2962=VERTEX_POINT('',#9604);
#2963=VERTEX_POINT('',#9606);
#3572=EDGE_CURVE('',#2960,#2960,#2591,.T.);
#3573=EDGE_CURVE('',#2960,#2961,#1884,.T.);
#3574=EDGE_CURVE('',#2961,#2961,#2592,.T.);
#3575=EDGE_CURVE('',#2962,#2962,#2593,.T.);
#3576=EDGE_CURVE('',#2962,#2963,#1885,.T.);
#3577=EDGE_CURVE('',#2963,#2963,#2594,.T.);
#4748=ORIENTED_EDGE('',*,*,#3572,.F.);
#4749=ORIENTED_EDGE('',*,*,#3573,.T.);
#4750=ORIENTED_EDGE('',*,*,#3574,.T.);
#4751=ORIENTED_EDGE('',*,*,#3573,.F.);
#4752=ORIENTED_EDGE('',*,*,#3575,.F.);
#4753=ORIENTED_EDGE('',*,*,#3576,.T.);
#4754=ORIENTED_EDGE('',*,*,#3577,.T.);
#4755=ORIENTED_EDGE('',*,*,#3576,.F.);
#4756=ORIENTED_EDGE('',*,*,#3575,.T.);
#4757=ORIENTED_EDGE('',*,*,#3572,.T.);
#4758=ORIENTED_EDGE('',*,*,#3577,.F.);
#4759=ORIENTED_EDGE('',*,*,#3574,.F.);
#5174=CYLINDRICAL_SURFACE('',#6452,0.42);
#5175=CYLINDRICAL_SURFACE('',#6455,0.8);
#5436=ADVANCED_FACE('',(#1087),#5174,.F.);
#5437=ADVANCED_FACE('',(#1088),#5175,.T.);
#5438=ADVANCED_FACE('',(#1089,#622),#771,.T.);
#5439=ADVANCED_FACE('',(#1090,#623),#772,.F.);
#5543=CLOSED_SHELL('',(#5436,#5437,#5438,#5439));
#6451=AXIS2_PLACEMENT_3D('',#9596,#7972,#7973);
#6452=AXIS2_PLACEMENT_3D('',#9597,#7974,#7975);
#6453=AXIS2_PLACEMENT_3D('',#9599,#7976,#7977);
#6454=AXIS2_PLACEMENT_3D('',#9602,#7979,#7980);
#6455=AXIS2_PLACEMENT_3D('',#9603,#7981,#7982);
#6456=AXIS2_PLACEMENT_3D('',#9605,#7983,#7984);
#6457=AXIS2_PLACEMENT_3D('',#9608,#7986,#7987);
#6458=AXIS2_PLACEMENT_3D('',#9609,#7988,#7989);
#6459=AXIS2_PLACEMENT_3D('',#9610,#7990,#7991);
#7972=DIRECTION('axis',(0.,0.,1.));
#7973=DIRECTION('refdir',(1.,0.,0.));
#7974=DIRECTION('center_axis',(0.,1.,0.));
#7975=DIRECTION('ref_axis',(1.,0.,0.));
#7976=DIRECTION('center_axis',(0.,-1.,0.));
#7977=DIRECTION('ref_axis',(1.,0.,0.));
#7978=DIRECTION('',(0.,-1.,0.));
#7979=DIRECTION('center_axis',(0.,-1.,0.));
#7980=DIRECTION('ref_axis',(1.,0.,0.));
#7981=DIRECTION('center_axis',(0.,1.,0.));
#7982=DIRECTION('ref_axis',(1.,0.,0.));
#7983=DIRECTION('center_axis',(0.,1.,0.));
#7984=DIRECTION('ref_axis',(1.,0.,0.));
#7985=DIRECTION('',(0.,-1.,0.));
#7986=DIRECTION('center_axis',(0.,1.,0.));
#7987=DIRECTION('ref_axis',(1.,0.,0.));
#7988=DIRECTION('center_axis',(0.,1.,0.));
#7989=DIRECTION('ref_axis',(1.,0.,0.));
#7990=DIRECTION('center_axis',(0.,1.,0.));
#7991=DIRECTION('ref_axis',(1.,0.,0.));
#9596=CARTESIAN_POINT('',(0.,0.,0.));
#9597=CARTESIAN_POINT('Origin',(0.,0.,0.));
#9598=CARTESIAN_POINT('',(-0.42,0.16,5.14351655641888E-17));
#9599=CARTESIAN_POINT('Origin',(0.,0.16,0.));
#9600=CARTESIAN_POINT('',(-0.42,0.,5.14351655641888E-17));
#9601=CARTESIAN_POINT('',(-0.42,0.,5.14351655641888E-17));
#9602=CARTESIAN_POINT('Origin',(0.,0.,0.));
#9603=CARTESIAN_POINT('Origin',(0.,0.,0.));
#9604=CARTESIAN_POINT('',(-0.8,0.16,9.79717439317883E-17));
#9605=CARTESIAN_POINT('Origin',(0.,0.16,0.));
#9606=CARTESIAN_POINT('',(-0.8,0.,9.79717439317883E-17));
#9607=CARTESIAN_POINT('',(-0.8,0.,9.79717439317883E-17));
#9608=CARTESIAN_POINT('Origin',(0.,0.,0.));
#9609=CARTESIAN_POINT('Origin',(0.,0.16,0.));
#9610=CARTESIAN_POINT('Origin',(0.,0.,0.));
#10049=UNCERTAINTY_MEASURE_WITH_UNIT(LENGTH_MEASURE(0.001),#10096,
'DISTANCE_ACCURACY_VALUE',
'Maximum model space distance between geometric entities at asserted c
onnectivities');
#10058=UNCERTAINTY_MEASURE_WITH_UNIT(LENGTH_MEASURE(0.001),#10096,
'DISTANCE_ACCURACY_VALUE',
'Maximum model space distance between geometric entities at asserted c
onnectivities');
#10086=(
GEOMETRIC_REPRESENTATION_CONTEXT(3)
GLOBAL_UNCERTAINTY_ASSIGNED_CONTEXT((#10049))
GLOBAL_UNIT_ASSIGNED_CONTEXT((#10096,#10098,#10099))
REPRESENTATION_CONTEXT('','3D')
);
#10095=(
GEOMETRIC_REPRESENTATION_CONTEXT(3)
GLOBAL_UNCERTAINTY_ASSIGNED_CONTEXT((#10058))
GLOBAL_UNIT_ASSIGNED_CONTEXT((#10096,#10098,#10099))
REPRESENTATION_CONTEXT('','3D')
);
#10096=(
LENGTH_UNIT()
NAMED_UNIT(*)
SI_UNIT(.CENTI.,.METRE.)
);
#10098=(
NAMED_UNIT(*)
PLANE_ANGLE_UNIT()
SI_UNIT($,.RADIAN.)
);
#10099=(
NAMED_UNIT(*)
SI_UNIT($,.STERADIAN.)
SOLID_ANGLE_UNIT()
);
#10127=SHAPE_DEFINITION_REPRESENTATION(#10198,#10274);
#10198=PRODUCT_DEFINITION_SHAPE('',$,#10311);
#10274=SHAPE_REPRESENTATION('',(#6451),#10086);
#10283=PRODUCT_DEFINITION_CONTEXT('part definition',#10393,'design');
#10311=PRODUCT_DEFINITION('Flat Washer - M8','Flat Washer - M8',#10347,
#10283);
#10347=PRODUCT_DEFINITION_FORMATION('',$,#10422);
#10393=APPLICATION_CONTEXT(
'Core Data for Automotive Mechanical Design Process');
#10394=PRODUCT_CONTEXT('part definition',#10393,'mechanical');
#10422=PRODUCT('Flat Washer - M8','Flat Washer - M8','Flat Washer - M8',
(#10394));
#10501=COLOUR_RGB('Black',0.12,0.14,0.17);
#10502=FILL_AREA_STYLE_COLOUR('',#10501);
#10503=FILL_AREA_STYLE('',(#10502));
#10504=SURFACE_STYLE_FILL_AREA(#10503);
#10505=SURFACE_SIDE_STYLE('',(#10504));
#10506=SURFACE_STYLE_USAGE(.BOTH.,#10505);
#10507=PRESENTATION_STYLE_ASSIGNMENT((#10506));
ENDSEC;
END-ISO-10303-21;
